ISO-10303-21;
HEADER;
/* Generated by software containing ST-Developer
 * from STEP Tools, Inc. (www.steptools.com) 
 */

FILE_DESCRIPTION(
/* description */ ('Compact handwheel screw vise'),
/* implementation_level */ '2;1');

FILE_NAME(
/* name */ 'Cap Screw - M5x20.step',
/* time_stamp */ '2026-10-29T16:08:22-07:00',
/* author */ (''),
/* organization */ (''),
/* preprocessor_version */ 'ST-DEVELOPER v20.2',
/* originating_system */ 'Autodesk Translation Framework v15.17.0.0',
/* authorisation */ '');

FILE_SCHEMA (('AUTOMOTIVE_DESIGN { 1 0 10303 214 3 1 1 }'));
ENDSEC;

DATA;
#10=MECHANICAL_DESIGN_GEOMETRIC_PRESENTATION_REPRESENTATION('',(#668),#25074);
#566=CONICAL_SURFACE('',#8831,0.4,0.785398163397448);
#567=CONICAL_SURFACE('',#8835,0.41,0.785398163397448);
#568=CONICAL_SURFACE('',#8839,0.26,0.463647609000806);
#569=CONICAL_SURFACE('',#8843,0.225,0.785398163397448);
#581=ORIENTED_CLOSED_SHELL('',*,#8078,.F.);
#585=BREP_WITH_VOIDS('Body1',#8077,(#581));
#604=SHAPE_REPRESENTATION_RELATIONSHIP('SRR','None',#25214,#632);
#632=ADVANCED_BREP_SHAPE_REPRESENTATION('',(#585),#25061);
#668=STYLED_ITEM('',(#25446),#585);
#797=FACE_BOUND('',#1792,.T.);
#931=PLANE('',#8829);
#932=PLANE('',#8837);
#933=PLANE('',#8845);
#934=PLANE('',#8846);
#935=PLANE('',#8847);
#936=PLANE('',#8848);
#937=PLANE('',#8849);
#938=PLANE('',#8850);
#939=PLANE('',#8851);
#940=PLANE('',#8852);
#941=PLANE('',#8853);
#1232=FACE_OUTER_BOUND('',#1787,.T.);
#1233=FACE_OUTER_BOUND('',#1788,.T.);
#1234=FACE_OUTER_BOUND('',#1789,.T.);
#1235=FACE_OUTER_BOUND('',#1790,.T.);
#1236=FACE_OUTER_BOUND('',#1791,.T.);
#1237=FACE_OUTER_BOUND('',#1793,.T.);
#1238=FACE_OUTER_BOUND('',#1794,.T.);
#1239=FACE_OUTER_BOUND('',#1795,.T.);
#1240=FACE_OUTER_BOUND('',#1796,.T.);
#1241=FACE_OUTER_BOUND('',#1797,.T.);
#1242=FACE_OUTER_BOUND('',#1798,.T.);
#1243=FACE_OUTER_BOUND('',#1799,.T.);
#1244=FACE_OUTER_BOUND('',#1800,.T.);
#1245=FACE_OUTER_BOUND('',#1801,.T.);
#1246=FACE_OUTER_BOUND('',#1802,.T.);
#1247=FACE_OUTER_BOUND('',#1803,.T.);
#1248=FACE_OUTER_BOUND('',#1804,.T.);
#1787=EDGE_LOOP('',(#6091));
#1788=EDGE_LOOP('',(#6092,#6093,#6094,#6095));
#1789=EDGE_LOOP('',(#6096,#6097,#6098,#6099));
#1790=EDGE_LOOP('',(#6100,#6101,#6102,#6103));
#1791=EDGE_LOOP('',(#6104));
#1792=EDGE_LOOP('',(#6105));
#1793=EDGE_LOOP('',(#6106,#6107,#6108,#6109));
#1794=EDGE_LOOP('',(#6110,#6111,#6112,#6113));
#1795=EDGE_LOOP('',(#6114,#6115,#6116,#6117));
#1796=EDGE_LOOP('',(#6118));
#1797=EDGE_LOOP('',(#6119,#6120,#6121,#6122));
#1798=EDGE_LOOP('',(#6123,#6124,#6125,#6126));
#1799=EDGE_LOOP('',(#6127,#6128,#6129,#6130));
#1800=EDGE_LOOP('',(#6131,#6132,#6133,#6134));
#1801=EDGE_LOOP('',(#6135,#6136,#6137,#6138));
#1802=EDGE_LOOP('',(#6139,#6140,#6141,#6142));
#1803=EDGE_LOOP('',(#6143,#6144,#6145,#6146,#6147,#6148));
#1804=EDGE_LOOP('',(#6149,#6150,#6151,#6152,#6153,#6154));
#2283=LINE('',#14722,#2791);
#2284=LINE('',#14726,#2792);
#2285=LINE('',#14730,#2793);
#2286=LINE('',#14737,#2794);
#2287=LINE('',#14741,#2795);
#2288=LINE('',#14745,#2796);
#2289=LINE('',#14750,#2797);
#2290=LINE('',#14752,#2798);
#2291=LINE('',#14754,#2799);
#2292=LINE('',#14755,#2800);
#2293=LINE('',#14758,#2801);
#2294=LINE('',#14760,#2802);
#2295=LINE('',#14761,#2803);
#2296=LINE('',#14764,#2804);
#2297=LINE('',#14766,#2805);
#2298=LINE('',#14767,#2806);
#2299=LINE('',#14770,#2807);
#2300=LINE('',#14772,#2808);
#2301=LINE('',#14773,#2809);
#2302=LINE('',#14776,#2810);
#2303=LINE('',#14778,#2811);
#2304=LINE('',#14779,#2812);
#2305=LINE('',#14781,#2813);
#2306=LINE('',#14782,#2814);
#2791=VECTOR('',#10289,0.4);
#2792=VECTOR('',#10294,0.425);
#2793=VECTOR('',#10299,0.41);
#2794=VECTOR('',#10308,0.26);
#2795=VECTOR('',#10313,0.25);
#2796=VECTOR('',#10318,0.225);
#2797=VECTOR('',#10323,1.);
#2798=VECTOR('',#10324,1.);
#2799=VECTOR('',#10325,1.);
#2800=VECTOR('',#10326,1.);
#2801=VECTOR('',#10329,1.);
#2802=VECTOR('',#10330,1.);
#2803=VECTOR('',#10331,1.);
#2804=VECTOR('',#10334,1.);
#2805=VECTOR('',#10335,1.);
#2806=VECTOR('',#10336,1.);
#2807=VECTOR('',#10339,1.);
#2808=VECTOR('',#10340,1.);
#2809=VECTOR('',#10341,1.);
#2810=VECTOR('',#10344,1.);
#2811=VECTOR('',#10345,1.);
#2812=VECTOR('',#10346,1.);
#2813=VECTOR('',#10349,1.);
#2814=VECTOR('',#10350,1.);
#3262=CIRCLE('',#8830,0.375);
#3263=CIRCLE('',#8832,0.425);
#3264=CIRCLE('',#8834,0.425);
#3265=CIRCLE('',#8836,0.395);
#3266=CIRCLE('',#8838,0.27);
#3267=CIRCLE('',#8840,0.24505);
#3268=CIRCLE('',#8842,0.24505);
#3269=CIRCLE('',#8844,0.2);
#3652=VERTEX_POINT('',#14717);
#3653=VERTEX_POINT('',#14720);
#3654=VERTEX_POINT('',#14724);
#3655=VERTEX_POINT('',#14728);
#3656=VERTEX_POINT('',#14732);
#3657=VERTEX_POINT('',#14735);
#3658=VERTEX_POINT('',#14739);
#3659=VERTEX_POINT('',#14743);
#3660=VERTEX_POINT('',#14748);
#3661=VERTEX_POINT('',#14749);
#3662=VERTEX_POINT('',#14751);
#3663=VERTEX_POINT('',#14753);
#3664=VERTEX_POINT('',#14757);
#3665=VERTEX_POINT('',#14759);
#3666=VERTEX_POINT('',#14763);
#3667=VERTEX_POINT('',#14765);
#3668=VERTEX_POINT('',#14769);
#3669=VERTEX_POINT('',#14771);
#3670=VERTEX_POINT('',#14775);
#3671=VERTEX_POINT('',#14777);
#4532=EDGE_CURVE('',#3652,#3652,#3262,.T.);
#4533=EDGE_CURVE('',#3653,#3653,#3263,.T.);
#4534=EDGE_CURVE('',#3653,#3652,#2283,.T.);
#4535=EDGE_CURVE('',#3654,#3654,#3264,.T.);
#4536=EDGE_CURVE('',#3654,#3653,#2284,.T.);
#4537=EDGE_CURVE('',#3655,#3655,#3265,.T.);
#4538=EDGE_CURVE('',#3655,#3654,#2285,.T.);
#4539=EDGE_CURVE('',#3656,#3656,#3266,.T.);
#4540=EDGE_CURVE('',#3657,#3657,#3267,.F.);
#4541=EDGE_CURVE('',#3657,#3656,#2286,.T.);
#4542=EDGE_CURVE('',#3658,#3658,#3268,.F.);
#4543=EDGE_CURVE('',#3658,#3657,#2287,.T.);
#4544=EDGE_CURVE('',#3659,#3659,#3269,.T.);
#4545=EDGE_CURVE('',#3659,#3658,#2288,.T.);
#4546=EDGE_CURVE('',#3660,#3661,#2289,.T.);
#4547=EDGE_CURVE('',#3661,#3662,#2290,.T.);
#4548=EDGE_CURVE('',#3662,#3663,#2291,.T.);
#4549=EDGE_CURVE('',#3660,#3663,#2292,.T.);
#4550=EDGE_CURVE('',#3661,#3664,#2293,.T.);
#4551=EDGE_CURVE('',#3664,#3665,#2294,.T.);
#4552=EDGE_CURVE('',#3665,#3662,#2295,.T.);
#4553=EDGE_CURVE('',#3664,#3666,#2296,.T.);
#4554=EDGE_CURVE('',#3666,#3667,#2297,.T.);
#4555=EDGE_CURVE('',#3667,#3665,#2298,.T.);
#4556=EDGE_CURVE('',#3666,#3668,#2299,.T.);
#4557=EDGE_CURVE('',#3668,#3669,#2300,.T.);
#4558=EDGE_CURVE('',#3669,#3667,#2301,.T.);
#4559=EDGE_CURVE('',#3668,#3670,#2302,.T.);
#4560=EDGE_CURVE('',#3670,#3671,#2303,.T.);
#4561=EDGE_CURVE('',#3671,#3669,#2304,.T.);
#4562=EDGE_CURVE('',#3670,#3660,#2305,.T.);
#4563=EDGE_CURVE('',#3663,#3671,#2306,.T.);
#6091=ORIENTED_EDGE('',*,*,#4532,.F.);
#6092=ORIENTED_EDGE('',*,*,#4533,.F.);
#6093=ORIENTED_EDGE('',*,*,#4534,.T.);
#6094=ORIENTED_EDGE('',*,*,#4532,.T.);
#6095=ORIENTED_EDGE('',*,*,#4534,.F.);
#6096=ORIENTED_EDGE('',*,*,#4535,.F.);
#6097=ORIENTED_EDGE('',*,*,#4536,.T.);
#6098=ORIENTED_EDGE('',*,*,#4533,.T.);
#6099=ORIENTED_EDGE('',*,*,#4536,.F.);
#6100=ORIENTED_EDGE('',*,*,#4537,.F.);
#6101=ORIENTED_EDGE('',*,*,#4538,.T.);
#6102=ORIENTED_EDGE('',*,*,#4535,.T.);
#6103=ORIENTED_EDGE('',*,*,#4538,.F.);
#6104=ORIENTED_EDGE('',*,*,#4537,.T.);
#6105=ORIENTED_EDGE('',*,*,#4539,.F.);
#6106=ORIENTED_EDGE('',*,*,#4540,.F.);
#6107=ORIENTED_EDGE('',*,*,#4541,.T.);
#6108=ORIENTED_EDGE('',*,*,#4539,.T.);
#6109=ORIENTED_EDGE('',*,*,#4541,.F.);
#6110=ORIENTED_EDGE('',*,*,#4542,.F.);
#6111=ORIENTED_EDGE('',*,*,#4543,.T.);
#6112=ORIENTED_EDGE('',*,*,#4540,.T.);
#6113=ORIENTED_EDGE('',*,*,#4543,.F.);
#6114=ORIENTED_EDGE('',*,*,#4544,.F.);
#6115=ORIENTED_EDGE('',*,*,#4545,.T.);
#6116=ORIENTED_EDGE('',*,*,#4542,.T.);
#6117=ORIENTED_EDGE('',*,*,#4545,.F.);
#6118=ORIENTED_EDGE('',*,*,#4544,.T.);
#6119=ORIENTED_EDGE('',*,*,#4546,.T.);
#6120=ORIENTED_EDGE('',*,*,#4547,.T.);
#6121=ORIENTED_EDGE('',*,*,#4548,.T.);
#6122=ORIENTED_EDGE('',*,*,#4549,.F.);
#6123=ORIENTED_EDGE('',*,*,#4550,.T.);
#6124=ORIENTED_EDGE('',*,*,#4551,.T.);
#6125=ORIENTED_EDGE('',*,*,#4552,.T.);
#6126=ORIENTED_EDGE('',*,*,#4547,.F.);
#6127=ORIENTED_EDGE('',*,*,#4553,.T.);
#6128=ORIENTED_EDGE('',*,*,#4554,.T.);
#6129=ORIENTED_EDGE('',*,*,#4555,.T.);
#6130=ORIENTED_EDGE('',*,*,#4551,.F.);
#6131=ORIENTED_EDGE('',*,*,#4556,.T.);
#6132=ORIENTED_EDGE('',*,*,#4557,.T.);
#6133=ORIENTED_EDGE('',*,*,#4558,.T.);
#6134=ORIENTED_EDGE('',*,*,#4554,.F.);
#6135=ORIENTED_EDGE('',*,*,#4559,.T.);
#6136=ORIENTED_EDGE('',*,*,#4560,.T.);
#6137=ORIENTED_EDGE('',*,*,#4561,.T.);
#6138=ORIENTED_EDGE('',*,*,#4557,.F.);
#6139=ORIENTED_EDGE('',*,*,#4562,.T.);
#6140=ORIENTED_EDGE('',*,*,#4549,.T.);
#6141=ORIENTED_EDGE('',*,*,#4563,.T.);
#6142=ORIENTED_EDGE('',*,*,#4560,.F.);
#6143=ORIENTED_EDGE('',*,*,#4562,.F.);
#6144=ORIENTED_EDGE('',*,*,#4559,.F.);
#6145=ORIENTED_EDGE('',*,*,#4556,.F.);
#6146=ORIENTED_EDGE('',*,*,#4553,.F.);
#6147=ORIENTED_EDGE('',*,*,#4550,.F.);
#6148=ORIENTED_EDGE('',*,*,#4546,.F.);
#6149=ORIENTED_EDGE('',*,*,#4563,.F.);
#6150=ORIENTED_EDGE('',*,*,#4548,.F.);
#6151=ORIENTED_EDGE('',*,*,#4552,.F.);
#6152=ORIENTED_EDGE('',*,*,#4555,.F.);
#6153=ORIENTED_EDGE('',*,*,#4558,.F.);
#6154=ORIENTED_EDGE('',*,*,#4561,.F.);
#7429=CYLINDRICAL_SURFACE('',#8833,0.425);
#7430=CYLINDRICAL_SURFACE('',#8841,0.24505);
#7802=ADVANCED_FACE('',(#1232),#931,.T.);
#7803=ADVANCED_FACE('',(#1233),#566,.T.);
#7804=ADVANCED_FACE('',(#1234),#7429,.T.);
#7805=ADVANCED_FACE('',(#1235),#567,.T.);
#7806=ADVANCED_FACE('',(#1236,#797),#932,.T.);
#7807=ADVANCED_FACE('',(#1237),#568,.T.);
#7808=ADVANCED_FACE('',(#1238),#7430,.T.);
#7809=ADVANCED_FACE('',(#1239),#569,.T.);
#7810=ADVANCED_FACE('',(#1240),#933,.T.);
#7811=ADVANCED_FACE('',(#1241),#934,.F.);
#7812=ADVANCED_FACE('',(#1242),#935,.F.);
#7813=ADVANCED_FACE('',(#1243),#936,.F.);
#7814=ADVANCED_FACE('',(#1244),#937,.F.);
#7815=ADVANCED_FACE('',(#1245),#938,.F.);
#7816=ADVANCED_FACE('',(#1246),#939,.F.);
#7817=ADVANCED_FACE('',(#1247),#940,.F.);
#7818=ADVANCED_FACE('',(#1248),#941,.F.);
#8077=CLOSED_SHELL('',(#7802,#7803,#7804,#7805,#7806,#7807,#7808,#7809,
#7810));
#8078=CLOSED_SHELL('',(#7811,#7812,#7813,#7814,#7815,#7816,#7817,#7818));
#8828=AXIS2_PLACEMENT_3D('',#14715,#10279,#10280);
#8829=AXIS2_PLACEMENT_3D('',#14716,#10281,#10282);
#8830=AXIS2_PLACEMENT_3D('',#14718,#10283,#10284);
#8831=AXIS2_PLACEMENT_3D('',#14719,#10285,#10286);
#8832=AXIS2_PLACEMENT_3D('',#14721,#10287,#10288);
#8833=AXIS2_PLACEMENT_3D('',#14723,#10290,#10291);
#8834=AXIS2_PLACEMENT_3D('',#14725,#10292,#10293);
#8835=AXIS2_PLACEMENT_3D('',#14727,#10295,#10296);
#8836=AXIS2_PLACEMENT_3D('',#14729,#10297,#10298);
#8837=AXIS2_PLACEMENT_3D('',#14731,#10300,#10301);
#8838=AXIS2_PLACEMENT_3D('',#14733,#10302,#10303);
#8839=AXIS2_PLACEMENT_3D('',#14734,#10304,#10305);
#8840=AXIS2_PLACEMENT_3D('',#14736,#10306,#10307);
#8841=AXIS2_PLACEMENT_3D('',#14738,#10309,#10310);
#8842=AXIS2_PLACEMENT_3D('',#14740,#10311,#10312);
#8843=AXIS2_PLACEMENT_3D('',#14742,#10314,#10315);
#8844=AXIS2_PLACEMENT_3D('',#14744,#10316,#10317);
#8845=AXIS2_PLACEMENT_3D('',#14746,#10319,#10320);
#8846=AXIS2_PLACEMENT_3D('',#14747,#10321,#10322);
#8847=AXIS2_PLACEMENT_3D('',#14756,#10327,#10328);
#8848=AXIS2_PLACEMENT_3D('',#14762,#10332,#10333);
#8849=AXIS2_PLACEMENT_3D('',#14768,#10337,#10338);
#8850=AXIS2_PLACEMENT_3D('',#14774,#10342,#10343);
#8851=AXIS2_PLACEMENT_3D('',#14780,#10347,#10348);
#8852=AXIS2_PLACEMENT_3D('',#14783,#10351,#10352);
#8853=AXIS2_PLACEMENT_3D('',#14784,#10353,#10354);
#10279=DIRECTION('axis',(0.,0.,1.));
#10280=DIRECTION('refdir',(1.,0.,0.));
#10281=DIRECTION('center_axis',(0.,1.,0.));
#10282=DIRECTION('ref_axis',(0.,0.,1.));
#10283=DIRECTION('center_axis',(0.,-1.,0.));
#10284=DIRECTION('ref_axis',(1.,0.,0.));
#10285=DIRECTION('center_axis',(0.,-1.,0.));
#10286=DIRECTION('ref_axis',(1.,0.,0.));
#10287=DIRECTION('center_axis',(0.,-1.,0.));
#10288=DIRECTION('ref_axis',(1.,0.,0.));
#10289=DIRECTION('',(0.707106781186548,0.707106781186547,8.65956056235493E-17));
#10290=DIRECTION('center_axis',(0.,-1.,0.));
#10291=DIRECTION('ref_axis',(1.,0.,0.));
#10292=DIRECTION('center_axis',(0.,-1.,0.));
#10293=DIRECTION('ref_axis',(1.,0.,0.));
#10294=DIRECTION('',(0.,1.,0.));
#10295=DIRECTION('center_axis',(0.,1.,0.));
#10296=DIRECTION('ref_axis',(1.,0.,0.));
#10297=DIRECTION('center_axis',(0.,-1.,0.));
#10298=DIRECTION('ref_axis',(1.,0.,0.));
#10299=DIRECTION('',(-0.707106781186547,0.707106781186548,-8.65956056235493E-17));
#10300=DIRECTION('center_axis',(0.,-1.,0.));
#10301=DIRECTION('ref_axis',(0.,0.,-1.));
#10302=DIRECTION('center_axis',(0.,-1.,0.));
#10303=DIRECTION('ref_axis',(1.,0.,0.));
#10304=DIRECTION('center_axis',(0.,1.,0.));
#10305=DIRECTION('ref_axis',(1.,0.,0.));
#10306=DIRECTION('center_axis',(0.,1.,0.));
#10307=DIRECTION('ref_axis',(1.,0.,0.));
#10308=DIRECTION('',(-0.447213595499958,0.894427190999916,-5.47678698264203E-17));
#10309=DIRECTION('center_axis',(0.,-1.,0.));
#10310=DIRECTION('ref_axis',(1.,0.,0.));
#10311=DIRECTION('center_axis',(0.,1.,0.));
#10312=DIRECTION('ref_axis',(1.,0.,0.));
#10313=DIRECTION('',(0.,1.,0.));
#10314=DIRECTION('center_axis',(0.,1.,0.));
#10315=DIRECTION('ref_axis',(1.,0.,0.));
#10316=DIRECTION('center_axis',(0.,-1.,0.));
#10317=DIRECTION('ref_axis',(1.,0.,0.));
#10318=DIRECTION('',(-0.707106781186547,0.707106781186548,-8.65956056235493E-17));
#10319=DIRECTION('center_axis',(0.,-1.,0.));
#10320=DIRECTION('ref_axis',(0.,0.,-1.));
#10321=DIRECTION('center_axis',(0.866025403784439,0.,-0.5));
#10322=DIRECTION('ref_axis',(0.5,0.,0.866025403784439));
#10323=DIRECTION('',(-0.5,0.,-0.866025403784439));
#10324=DIRECTION('',(0.,-1.,0.));
#10325=DIRECTION('',(0.5,0.,0.866025403784439));
#10326=DIRECTION('',(0.,-1.,0.));
#10327=DIRECTION('center_axis',(1.20185167898973E-16,0.,-1.));
#10328=DIRECTION('ref_axis',(1.,0.,1.20185167898973E-16));
#10329=DIRECTION('',(-1.,0.,-1.20185167898973E-16));
#10330=DIRECTION('',(0.,-1.,0.));
#10331=DIRECTION('',(1.,0.,1.20185167898973E-16));
#10332=DIRECTION('center_axis',(-0.866025403784439,0.,-0.5));
#10333=DIRECTION('ref_axis',(0.5,0.,-0.866025403784439));
#10334=DIRECTION('',(-0.5,0.,0.866025403784439));
#10335=DIRECTION('',(0.,-1.,0.));
#10336=DIRECTION('',(0.5,0.,-0.866025403784439));
#10337=DIRECTION('center_axis',(-0.866025403784439,0.,0.5));
#10338=DIRECTION('ref_axis',(-0.5,0.,-0.866025403784439));
#10339=DIRECTION('',(0.5,0.,0.866025403784439));
#10340=DIRECTION('',(0.,-1.,0.));
#10341=DIRECTION('',(-0.5,0.,-0.866025403784439));
#10342=DIRECTION('center_axis',(-2.40370335797945E-16,0.,1.));
#10343=DIRECTION('ref_axis',(-1.,0.,-2.40370335797945E-16));
#10344=DIRECTION('',(1.,0.,2.40370335797945E-16));
#10345=DIRECTION('',(0.,-1.,0.));
#10346=DIRECTION('',(-1.,0.,-2.40370335797945E-16));
#10347=DIRECTION('center_axis',(0.866025403784439,0.,0.5));
#10348=DIRECTION('ref_axis',(-0.5,0.,0.866025403784439));
#10349=DIRECTION('',(0.5,0.,-0.866025403784439));
#10350=DIRECTION('',(-0.5,0.,0.866025403784439));
#10351=DIRECTION('center_axis',(0.,1.,0.));
#10352=DIRECTION('ref_axis',(1.,0.,0.));
#10353=DIRECTION('center_axis',(0.,-1.,0.));
#10354=DIRECTION('ref_axis',(0.,0.,-1.));
#14715=CARTESIAN_POINT('',(0.,0.,0.));
#14716=CARTESIAN_POINT('Origin',(0.375,0.5,0.));
#14717=CARTESIAN_POINT('',(-0.375,0.5,-4.59242549680257E-17));
#14718=CARTESIAN_POINT('Origin',(0.,0.5,0.));
#14719=CARTESIAN_POINT('Origin',(0.,0.475,0.));
#14720=CARTESIAN_POINT('',(-0.425,0.45,-5.20474889637625E-17));
#14721=CARTESIAN_POINT('Origin',(0.,0.45,0.));
#14722=CARTESIAN_POINT('',(-0.4,0.475,-4.89858719658941E-17));
#14723=CARTESIAN_POINT('Origin',(0.,0.24,0.));
#14724=CARTESIAN_POINT('',(-0.425,0.0299999999999998,-5.20474889637625E-17));
#14725=CARTESIAN_POINT('Origin',(0.,0.0299999999999998,0.));
#14726=CARTESIAN_POINT('',(-0.425,0.24,-5.20474889637625E-17));
#14727=CARTESIAN_POINT('Origin',(0.,0.0150000000000001,0.));
#14728=CARTESIAN_POINT('',(-0.395,4.85722573273506E-17,-4.83735485663204E-17));
#14729=CARTESIAN_POINT('Origin',(0.,0.,0.));
#14730=CARTESIAN_POINT('',(-0.41,0.0150000000000001,-5.02105187650415E-17));
#14731=CARTESIAN_POINT('Origin',(0.27,0.,0.));
#14732=CARTESIAN_POINT('',(-0.27,0.,-3.30654635769785E-17));
#14733=CARTESIAN_POINT('Origin',(0.,0.,0.));
#14734=CARTESIAN_POINT('Origin',(0.,-0.02,0.));
#14735=CARTESIAN_POINT('',(-0.24505,-0.0498999999999999,3.00099698131059E-17));
#14736=CARTESIAN_POINT('Origin',(0.,-0.0498999999999999,0.));
#14737=CARTESIAN_POINT('',(-0.26,-0.02,-3.18408167778312E-17));
#14738=CARTESIAN_POINT('Origin',(0.,-0.995,0.));
#14739=CARTESIAN_POINT('',(-0.24505,-1.95495,3.00099698131059E-17));
#14740=CARTESIAN_POINT('Origin',(0.,-1.95495,0.));
#14741=CARTESIAN_POINT('',(-0.24505,-0.995,-3.00099698131059E-17));
#14742=CARTESIAN_POINT('Origin',(0.,-1.975,0.));
#14743=CARTESIAN_POINT('',(-0.2,-2.,-2.44929359829471E-17));
#14744=CARTESIAN_POINT('Origin',(0.,-2.,0.));
#14745=CARTESIAN_POINT('',(-0.225,-1.975,-2.75545529808154E-17));
#14746=CARTESIAN_POINT('Origin',(0.,-2.,0.));
#14747=CARTESIAN_POINT('Origin',(0.115470053837925,-0.5,-0.2));
#14748=CARTESIAN_POINT('',(0.23094010767585,-0.5,0.));
#14749=CARTESIAN_POINT('',(0.115470053837925,-0.5,-0.2));
#14750=CARTESIAN_POINT('',(0.23094010767585,-0.5,0.));
#14751=CARTESIAN_POINT('',(0.115470053837925,-0.8,-0.2));
#14752=CARTESIAN_POINT('',(0.115470053837925,-0.5,-0.2));
#14753=CARTESIAN_POINT('',(0.23094010767585,-0.8,0.));
#14754=CARTESIAN_POINT('',(0.23094010767585,-0.8,0.));
#14755=CARTESIAN_POINT('',(0.23094010767585,-0.5,0.));
#14756=CARTESIAN_POINT('Origin',(-0.115470053837925,-0.5,-0.2));
#14757=CARTESIAN_POINT('',(-0.115470053837925,-0.5,-0.2));
#14758=CARTESIAN_POINT('',(0.115470053837925,-0.5,-0.2));
#14759=CARTESIAN_POINT('',(-0.115470053837925,-0.8,-0.2));
#14760=CARTESIAN_POINT('',(-0.115470053837925,-0.5,-0.2));
#14761=CARTESIAN_POINT('',(0.115470053837925,-0.8,-0.2));
#14762=CARTESIAN_POINT('Origin',(-0.23094010767585,-0.5,-2.77555756156289E-17));
#14763=CARTESIAN_POINT('',(-0.23094010767585,-0.5,-2.82820063659975E-17));
#14764=CARTESIAN_POINT('',(-0.115470053837925,-0.5,-0.2));
#14765=CARTESIAN_POINT('',(-0.23094010767585,-0.8,-2.77555756156289E-17));
#14766=CARTESIAN_POINT('',(-0.23094010767585,-0.5,-2.82820063659975E-17));
#14767=CARTESIAN_POINT('',(-0.115470053837925,-0.8,-0.2));
#14768=CARTESIAN_POINT('Origin',(-0.115470053837925,-0.5,0.2));
#14769=CARTESIAN_POINT('',(-0.115470053837925,-0.5,0.2));
#14770=CARTESIAN_POINT('',(-0.23094010767585,-0.5,-2.82820063659975E-17));
#14771=CARTESIAN_POINT('',(-0.115470053837925,-0.8,0.2));
#14772=CARTESIAN_POINT('',(-0.115470053837925,-0.5,0.2));
#14773=CARTESIAN_POINT('',(-0.23094010767585,-0.8,-2.82820063659975E-17));
#14774=CARTESIAN_POINT('Origin',(0.115470053837925,-0.5,0.2));
#14775=CARTESIAN_POINT('',(0.115470053837925,-0.5,0.2));
#14776=CARTESIAN_POINT('',(-0.115470053837925,-0.5,0.2));
#14777=CARTESIAN_POINT('',(0.115470053837925,-0.8,0.2));
#14778=CARTESIAN_POINT('',(0.115470053837925,-0.5,0.2));
#14779=CARTESIAN_POINT('',(-0.115470053837925,-0.8,0.2));
#14780=CARTESIAN_POINT('Origin',(0.23094010767585,-0.5,0.));
#14781=CARTESIAN_POINT('',(0.115470053837925,-0.5,0.2));
#14782=CARTESIAN_POINT('',(0.115470053837925,-0.8,0.2));
#14783=CARTESIAN_POINT('Origin',(0.,-0.5,0.));
#14784=CARTESIAN_POINT('Origin',(0.,-0.8,0.));
#25027=UNCERTAINTY_MEASURE_WITH_UNIT(LENGTH_MEASURE(0.001),#25075,
'DISTANCE_ACCURACY_VALUE',
'Maximum model space distance between geometric entities at asserted c
onnectivities');
#25040=UNCERTAINTY_MEASURE_WITH_UNIT(LENGTH_MEASURE(0.001),#25075,
'DISTANCE_ACCURACY_VALUE',
'Maximum model space distance between geometric entities at asserted c
onnectivities');
#25061=(
GEOMETRIC_REPRESENTATION_CONTEXT(3)
GLOBAL_UNCERTAINTY_ASSIGNED_CONTEXT((#25027))
GLOBAL_UNIT_ASSIGNED_CONTEXT((#25075,#25077,#25078))
REPRESENTATION_CONTEXT('','3D')
);
#25074=(
GEOMETRIC_REPRESENTATION_CONTEXT(3)
GLOBAL_UNCERTAINTY_ASSIGNED_CONTEXT((#25040))
GLOBAL_UNIT_ASSIGNED_CONTEXT((#25075,#25077,#25078))
REPRESENTATION_CONTEXT('','3D')
);
#25075=(
LENGTH_UNIT()
NAMED_UNIT(*)
SI_UNIT(.CENTI.,.METRE.)
);
#25077=(
NAMED_UNIT(*)
PLANE_ANGLE_UNIT()
SI_UNIT($,.RADIAN.)
);
#25078=(
NAMED_UNIT(*)
SI_UNIT($,.STERADIAN.)
SOLID_ANGLE_UNIT()
);
#25099=SHAPE_DEFINITION_REPRESENTATION(#25137,#25214);
#25137=PRODUCT_DEFINITION_SHAPE('',$,#25248);
#25214=SHAPE_REPRESENTATION('',(#8828),#25061);
#25227=PRODUCT_DEFINITION_CONTEXT('part definition',#25328,'design');
#25248=PRODUCT_DEFINITION('Cap Screw - M5x20','Cap Screw - M5x20',#25281,
#25227);
#25281=PRODUCT_DEFINITION_FORMATION('',$,#25350);
#25328=APPLICATION_CONTEXT(
'Core Data for Automotive Mechanical Design Process');
#25329=PRODUCT_CONTEXT('part definition',#25328,'mechanical');
#25350=PRODUCT('Cap Screw - M5x20','Cap Screw - M5x20',
'Cap Screw - M5x20',(#25329));
#25440=COLOUR_RGB('Black',0.12,0.14,0.17);
#25441=FILL_AREA_STYLE_COLOUR('',#25440);
#25442=FILL_AREA_STYLE('',(#25441));
#25443=SURFACE_STYLE_FILL_AREA(#25442);
#25444=SURFACE_SIDE_STYLE('',(#25443));
#25445=SURFACE_STYLE_USAGE(.BOTH.,#25444);
#25446=PRESENTATION_STYLE_ASSIGNMENT((#25445));
ENDSEC;
END-ISO-10303-21;
